ISO-10303-21;
HEADER;
/* Generated by software containing ST-Developer
 * from STEP Tools, Inc. (www.steptools.com) 
 */

FILE_DESCRIPTION(
/* description */ ('Door-style hinge test fixture with detent'),
/* implementation_level */ '2;1');

FILE_NAME(
/* name */ 'M6x18 mounting screw.step',
/* time_stamp */ '2026-10-28T03:24:57-07:00',
/* author */ (''),
/* organization */ (''),
/* preprocessor_version */ 'ST-DEVELOPER v20.2',
/* originating_system */ 'Autodesk Translation Framework v15.17.0.0',
/* authorisation */ '');

FILE_SCHEMA (('AUTOMOTIVE_DESIGN { 1 0 10303 214 3 1 1 }'));
ENDSEC;

DATA;
#10=MECHANICAL_DESIGN_GEOMETRIC_PRESENTATION_REPRESENTATION('',(#341),#9813);
#201=CONICAL_SURFACE('',#5431,0.475,0.785398163397449);
#202=CONICAL_SURFACE('',#5435,0.485,0.785398163397448);
#203=CONICAL_SURFACE('',#5439,0.31,0.463647609000806);
#215=ORIENTED_CLOSED_SHELL('',*,#4772,.F.);
#218=BREP_WITH_VOIDS('Body1',#4773,(#215));
#278=SHAPE_REPRESENTATION_RELATIONSHIP('SRR','None',#9955,#309);
#309=ADVANCED_BREP_SHAPE_REPRESENTATION('',(#218),#9798);
#341=STYLED_ITEM('',(#10190),#218);
#467=FACE_BOUND('',#1176,.T.);
#594=PLANE('',#5419);
#595=PLANE('',#5420);
#596=PLANE('',#5421);
#597=PLANE('',#5422);
#598=PLANE('',#5423);
#599=PLANE('',#5424);
#600=PLANE('',#5425);
#601=PLANE('',#5426);
#602=PLANE('',#5427);
#603=PLANE('',#5429);
#604=PLANE('',#5437);
#809=FACE_OUTER_BOUND('',#1162,.T.);
#810=FACE_OUTER_BOUND('',#1163,.T.);
#811=FACE_OUTER_BOUND('',#1164,.T.);
#812=FACE_OUTER_BOUND('',#1165,.T.);
#813=FACE_OUTER_BOUND('',#1166,.T.);
#814=FACE_OUTER_BOUND('',#1167,.T.);
#815=FACE_OUTER_BOUND('',#1168,.T.);
#816=FACE_OUTER_BOUND('',#1169,.T.);
#817=FACE_OUTER_BOUND('',#1170,.T.);
#818=FACE_OUTER_BOUND('',#1171,.T.);
#819=FACE_OUTER_BOUND('',#1172,.T.);
#820=FACE_OUTER_BOUND('',#1173,.T.);
#821=FACE_OUTER_BOUND('',#1174,.T.);
#822=FACE_OUTER_BOUND('',#1175,.T.);
#823=FACE_OUTER_BOUND('',#1177,.T.);
#824=FACE_OUTER_BOUND('',#1178,.T.);
#1162=EDGE_LOOP('',(#3839,#3840,#3841,#3842));
#1163=EDGE_LOOP('',(#3843,#3844,#3845,#3846));
#1164=EDGE_LOOP('',(#3847,#3848,#3849,#3850));
#1165=EDGE_LOOP('',(#3851,#3852,#3853,#3854));
#1166=EDGE_LOOP('',(#3855,#3856,#3857,#3858));
#1167=EDGE_LOOP('',(#3859,#3860,#3861,#3862));
#1168=EDGE_LOOP('',(#3863,#3864,#3865,#3866,#3867,#3868));
#1169=EDGE_LOOP('',(#3869,#3870,#3871,#3872,#3873,#3874));
#1170=EDGE_LOOP('',(#3875));
#1171=EDGE_LOOP('',(#3876));
#1172=EDGE_LOOP('',(#3877,#3878,#3879,#3880));
#1173=EDGE_LOOP('',(#3881,#3882,#3883,#3884));
#1174=EDGE_LOOP('',(#3885,#3886,#3887,#3888));
#1175=EDGE_LOOP('',(#3889));
#1176=EDGE_LOOP('',(#3890));
#1177=EDGE_LOOP('',(#3891,#3892,#3893,#3894));
#1178=EDGE_LOOP('',(#3895,#3896,#3897,#3898));
#1534=LINE('',#8708,#1854);
#1535=LINE('',#8710,#1855);
#1536=LINE('',#8712,#1856);
#1537=LINE('',#8713,#1857);
#1538=LINE('',#8716,#1858);
#1539=LINE('',#8718,#1859);
#1540=LINE('',#8719,#1860);
#1541=LINE('',#8722,#1861);
#1542=LINE('',#8724,#1862);
#1543=LINE('',#8725,#1863);
#1544=LINE('',#8728,#1864);
#1545=LINE('',#8730,#1865);
#1546=LINE('',#8731,#1866);
#1547=LINE('',#8734,#1867);
#1548=LINE('',#8736,#1868);
#1549=LINE('',#8737,#1869);
#1550=LINE('',#8739,#1870);
#1551=LINE('',#8740,#1871);
#1552=LINE('',#8752,#1872);
#1553=LINE('',#8756,#1873);
#1554=LINE('',#8760,#1874);
#1555=LINE('',#8767,#1875);
#1556=LINE('',#8769,#1876);
#1854=VECTOR('',#6515,1.);
#1855=VECTOR('',#6516,1.);
#1856=VECTOR('',#6517,1.);
#1857=VECTOR('',#6518,1.);
#1858=VECTOR('',#6521,1.);
#1859=VECTOR('',#6522,1.);
#1860=VECTOR('',#6523,1.);
#1861=VECTOR('',#6526,1.);
#1862=VECTOR('',#6527,1.);
#1863=VECTOR('',#6528,1.);
#1864=VECTOR('',#6531,1.);
#1865=VECTOR('',#6532,1.);
#1866=VECTOR('',#6533,1.);
#1867=VECTOR('',#6536,1.);
#1868=VECTOR('',#6537,1.);
#1869=VECTOR('',#6538,1.);
#1870=VECTOR('',#6541,1.);
#1871=VECTOR('',#6542,1.);
#1872=VECTOR('',#6559,0.475);
#1873=VECTOR('',#6564,0.5);
#1874=VECTOR('',#6569,0.485);
#1875=VECTOR('',#6578,0.31);
#1876=VECTOR('',#6581,0.3);
#2089=CIRCLE('',#5428,0.2942);
#2090=CIRCLE('',#5430,0.45);
#2091=CIRCLE('',#5432,0.5);
#2092=CIRCLE('',#5434,0.5);
#2093=CIRCLE('',#5436,0.47);
#2094=CIRCLE('',#5438,0.32);
#2095=CIRCLE('',#5440,0.2942);
#2433=VERTEX_POINT('',#8706);
#2434=VERTEX_POINT('',#8707);
#2435=VERTEX_POINT('',#8709);
#2436=VERTEX_POINT('',#8711);
#2437=VERTEX_POINT('',#8715);
#2438=VERTEX_POINT('',#8717);
#2439=VERTEX_POINT('',#8721);
#2440=VERTEX_POINT('',#8723);
#2441=VERTEX_POINT('',#8727);
#2442=VERTEX_POINT('',#8729);
#2443=VERTEX_POINT('',#8733);
#2444=VERTEX_POINT('',#8735);
#2445=VERTEX_POINT('',#8744);
#2446=VERTEX_POINT('',#8747);
#2447=VERTEX_POINT('',#8750);
#2448=VERTEX_POINT('',#8754);
#2449=VERTEX_POINT('',#8758);
#2450=VERTEX_POINT('',#8762);
#2451=VERTEX_POINT('',#8765);
#2936=EDGE_CURVE('',#2433,#2434,#1534,.T.);
#2937=EDGE_CURVE('',#2434,#2435,#1535,.T.);
#2938=EDGE_CURVE('',#2435,#2436,#1536,.T.);
#2939=EDGE_CURVE('',#2433,#2436,#1537,.T.);
#2940=EDGE_CURVE('',#2434,#2437,#1538,.T.);
#2941=EDGE_CURVE('',#2437,#2438,#1539,.T.);
#2942=EDGE_CURVE('',#2438,#2435,#1540,.T.);
#2943=EDGE_CURVE('',#2437,#2439,#1541,.T.);
#2944=EDGE_CURVE('',#2439,#2440,#1542,.T.);
#2945=EDGE_CURVE('',#2440,#2438,#1543,.T.);
#2946=EDGE_CURVE('',#2439,#2441,#1544,.T.);
#2947=EDGE_CURVE('',#2441,#2442,#1545,.T.);
#2948=EDGE_CURVE('',#2442,#2440,#1546,.T.);
#2949=EDGE_CURVE('',#2441,#2443,#1547,.T.);
#2950=EDGE_CURVE('',#2443,#2444,#1548,.T.);
#2951=EDGE_CURVE('',#2444,#2442,#1549,.T.);
#2952=EDGE_CURVE('',#2443,#2433,#1550,.T.);
#2953=EDGE_CURVE('',#2436,#2444,#1551,.T.);
#2954=EDGE_CURVE('',#2445,#2445,#2089,.T.);
#2955=EDGE_CURVE('',#2446,#2446,#2090,.T.);
#2956=EDGE_CURVE('',#2447,#2447,#2091,.T.);
#2957=EDGE_CURVE('',#2447,#2446,#1552,.T.);
#2958=EDGE_CURVE('',#2448,#2448,#2092,.T.);
#2959=EDGE_CURVE('',#2448,#2447,#1553,.T.);
#2960=EDGE_CURVE('',#2449,#2449,#2093,.T.);
#2961=EDGE_CURVE('',#2449,#2448,#1554,.T.);
#2962=EDGE_CURVE('',#2450,#2450,#2094,.T.);
#2963=EDGE_CURVE('',#2451,#2451,#2095,.F.);
#2964=EDGE_CURVE('',#2451,#2450,#1555,.T.);
#2965=EDGE_CURVE('',#2445,#2451,#1556,.T.);
#3839=ORIENTED_EDGE('',*,*,#2936,.T.);
#3840=ORIENTED_EDGE('',*,*,#2937,.T.);
#3841=ORIENTED_EDGE('',*,*,#2938,.T.);
#3842=ORIENTED_EDGE('',*,*,#2939,.F.);
#3843=ORIENTED_EDGE('',*,*,#2940,.T.);
#3844=ORIENTED_EDGE('',*,*,#2941,.T.);
#3845=ORIENTED_EDGE('',*,*,#2942,.T.);
#3846=ORIENTED_EDGE('',*,*,#2937,.F.);
#3847=ORIENTED_EDGE('',*,*,#2943,.T.);
#3848=ORIENTED_EDGE('',*,*,#2944,.T.);
#3849=ORIENTED_EDGE('',*,*,#2945,.T.);
#3850=ORIENTED_EDGE('',*,*,#2941,.F.);
#3851=ORIENTED_EDGE('',*,*,#2946,.T.);
#3852=ORIENTED_EDGE('',*,*,#2947,.T.);
#3853=ORIENTED_EDGE('',*,*,#2948,.T.);
#3854=ORIENTED_EDGE('',*,*,#2944,.F.);
#3855=ORIENTED_EDGE('',*,*,#2949,.T.);
#3856=ORIENTED_EDGE('',*,*,#2950,.T.);
#3857=ORIENTED_EDGE('',*,*,#2951,.T.);
#3858=ORIENTED_EDGE('',*,*,#2947,.F.);
#3859=ORIENTED_EDGE('',*,*,#2952,.T.);
#3860=ORIENTED_EDGE('',*,*,#2939,.T.);
#3861=ORIENTED_EDGE('',*,*,#2953,.T.);
#3862=ORIENTED_EDGE('',*,*,#2950,.F.);
#3863=ORIENTED_EDGE('',*,*,#2952,.F.);
#3864=ORIENTED_EDGE('',*,*,#2949,.F.);
#3865=ORIENTED_EDGE('',*,*,#2946,.F.);
#3866=ORIENTED_EDGE('',*,*,#2943,.F.);
#3867=ORIENTED_EDGE('',*,*,#2940,.F.);
#3868=ORIENTED_EDGE('',*,*,#2936,.F.);
#3869=ORIENTED_EDGE('',*,*,#2953,.F.);
#3870=ORIENTED_EDGE('',*,*,#2938,.F.);
#3871=ORIENTED_EDGE('',*,*,#2942,.F.);
#3872=ORIENTED_EDGE('',*,*,#2945,.F.);
#3873=ORIENTED_EDGE('',*,*,#2948,.F.);
#3874=ORIENTED_EDGE('',*,*,#2951,.F.);
#3875=ORIENTED_EDGE('',*,*,#2954,.F.);
#3876=ORIENTED_EDGE('',*,*,#2955,.F.);
#3877=ORIENTED_EDGE('',*,*,#2956,.F.);
#3878=ORIENTED_EDGE('',*,*,#2957,.T.);
#3879=ORIENTED_EDGE('',*,*,#2955,.T.);
#3880=ORIENTED_EDGE('',*,*,#2957,.F.);
#3881=ORIENTED_EDGE('',*,*,#2958,.F.);
#3882=ORIENTED_EDGE('',*,*,#2959,.T.);
#3883=ORIENTED_EDGE('',*,*,#2956,.T.);
#3884=ORIENTED_EDGE('',*,*,#2959,.F.);
#3885=ORIENTED_EDGE('',*,*,#2960,.F.);
#3886=ORIENTED_EDGE('',*,*,#2961,.T.);
#3887=ORIENTED_EDGE('',*,*,#2958,.T.);
#3888=ORIENTED_EDGE('',*,*,#2961,.F.);
#3889=ORIENTED_EDGE('',*,*,#2960,.T.);
#3890=ORIENTED_EDGE('',*,*,#2962,.F.);
#3891=ORIENTED_EDGE('',*,*,#2963,.F.);
#3892=ORIENTED_EDGE('',*,*,#2964,.T.);
#3893=ORIENTED_EDGE('',*,*,#2962,.T.);
#3894=ORIENTED_EDGE('',*,*,#2964,.F.);
#3895=ORIENTED_EDGE('',*,*,#2954,.T.);
#3896=ORIENTED_EDGE('',*,*,#2965,.T.);
#3897=ORIENTED_EDGE('',*,*,#2963,.T.);
#3898=ORIENTED_EDGE('',*,*,#2965,.F.);
#4431=CYLINDRICAL_SURFACE('',#5433,0.5);
#4432=CYLINDRICAL_SURFACE('',#5441,0.2942);
#4614=ADVANCED_FACE('',(#809),#594,.F.);
#4615=ADVANCED_FACE('',(#810),#595,.F.);
#4616=ADVANCED_FACE('',(#811),#596,.F.);
#4617=ADVANCED_FACE('',(#812),#597,.F.);
#4618=ADVANCED_FACE('',(#813),#598,.F.);
#4619=ADVANCED_FACE('',(#814),#599,.F.);
#4620=ADVANCED_FACE('',(#815),#600,.F.);
#4621=ADVANCED_FACE('',(#816),#601,.F.);
#4622=ADVANCED_FACE('',(#817),#602,.F.);
#4623=ADVANCED_FACE('',(#818),#603,.T.);
#4624=ADVANCED_FACE('',(#819),#201,.T.);
#4625=ADVANCED_FACE('',(#820),#4431,.T.);
#4626=ADVANCED_FACE('',(#821),#202,.T.);
#4627=ADVANCED_FACE('',(#822,#467),#604,.T.);
#4628=ADVANCED_FACE('',(#823),#203,.T.);
#4629=ADVANCED_FACE('',(#824),#4432,.T.);
#4772=CLOSED_SHELL('',(#4614,#4615,#4616,#4617,#4618,#4619,#4620,#4621));
#4773=CLOSED_SHELL('',(#4622,#4623,#4624,#4625,#4626,#4627,#4628,#4629));
#5418=AXIS2_PLACEMENT_3D('',#8704,#6511,#6512);
#5419=AXIS2_PLACEMENT_3D('',#8705,#6513,#6514);
#5420=AXIS2_PLACEMENT_3D('',#8714,#6519,#6520);
#5421=AXIS2_PLACEMENT_3D('',#8720,#6524,#6525);
#5422=AXIS2_PLACEMENT_3D('',#8726,#6529,#6530);
#5423=AXIS2_PLACEMENT_3D('',#8732,#6534,#6535);
#5424=AXIS2_PLACEMENT_3D('',#8738,#6539,#6540);
#5425=AXIS2_PLACEMENT_3D('',#8741,#6543,#6544);
#5426=AXIS2_PLACEMENT_3D('',#8742,#6545,#6546);
#5427=AXIS2_PLACEMENT_3D('',#8743,#6547,#6548);
#5428=AXIS2_PLACEMENT_3D('',#8745,#6549,#6550);
#5429=AXIS2_PLACEMENT_3D('',#8746,#6551,#6552);
#5430=AXIS2_PLACEMENT_3D('',#8748,#6553,#6554);
#5431=AXIS2_PLACEMENT_3D('',#8749,#6555,#6556);
#5432=AXIS2_PLACEMENT_3D('',#8751,#6557,#6558);
#5433=AXIS2_PLACEMENT_3D('',#8753,#6560,#6561);
#5434=AXIS2_PLACEMENT_3D('',#8755,#6562,#6563);
#5435=AXIS2_PLACEMENT_3D('',#8757,#6565,#6566);
#5436=AXIS2_PLACEMENT_3D('',#8759,#6567,#6568);
#5437=AXIS2_PLACEMENT_3D('',#8761,#6570,#6571);
#5438=AXIS2_PLACEMENT_3D('',#8763,#6572,#6573);
#5439=AXIS2_PLACEMENT_3D('',#8764,#6574,#6575);
#5440=AXIS2_PLACEMENT_3D('',#8766,#6576,#6577);
#5441=AXIS2_PLACEMENT_3D('',#8768,#6579,#6580);
#6511=DIRECTION('axis',(0.,0.,1.));
#6512=DIRECTION('refdir',(1.,0.,0.));
#6513=DIRECTION('center_axis',(0.866025403784439,0.,-0.5));
#6514=DIRECTION('ref_axis',(0.5,0.,0.866025403784439));
#6515=DIRECTION('',(-0.5,0.,-0.866025403784439));
#6516=DIRECTION('',(0.,-1.,0.));
#6517=DIRECTION('',(0.5,0.,0.866025403784439));
#6518=DIRECTION('',(0.,-1.,0.));
#6519=DIRECTION('center_axis',(1.92296268638356E-16,0.,-1.));
#6520=DIRECTION('ref_axis',(1.,0.,1.92296268638356E-16));
#6521=DIRECTION('',(-1.,0.,-1.92296268638356E-16));
#6522=DIRECTION('',(0.,-1.,0.));
#6523=DIRECTION('',(1.,0.,1.92296268638356E-16));
#6524=DIRECTION('center_axis',(-0.866025403784439,0.,-0.5));
#6525=DIRECTION('ref_axis',(0.5,0.,-0.866025403784439));
#6526=DIRECTION('',(-0.5,0.,0.866025403784438));
#6527=DIRECTION('',(0.,-1.,0.));
#6528=DIRECTION('',(0.5,0.,-0.866025403784438));
#6529=DIRECTION('center_axis',(-0.866025403784439,0.,0.5));
#6530=DIRECTION('ref_axis',(-0.5,0.,-0.866025403784439));
#6531=DIRECTION('',(0.5,0.,0.866025403784439));
#6532=DIRECTION('',(0.,-1.,0.));
#6533=DIRECTION('',(-0.5,0.,-0.866025403784439));
#6534=DIRECTION('center_axis',(-1.92296268638356E-16,0.,1.));
#6535=DIRECTION('ref_axis',(-1.,0.,-1.92296268638356E-16));
#6536=DIRECTION('',(1.,0.,1.92296268638356E-16));
#6537=DIRECTION('',(0.,-1.,0.));
#6538=DIRECTION('',(-1.,0.,-1.92296268638356E-16));
#6539=DIRECTION('center_axis',(0.866025403784439,0.,0.5));
#6540=DIRECTION('ref_axis',(-0.5,0.,0.866025403784439));
#6541=DIRECTION('',(0.5,0.,-0.866025403784439));
#6542=DIRECTION('',(-0.5,0.,0.866025403784439));
#6543=DIRECTION('center_axis',(0.,1.,0.));
#6544=DIRECTION('ref_axis',(1.,0.,0.));
#6545=DIRECTION('center_axis',(0.,-1.,0.));
#6546=DIRECTION('ref_axis',(0.,0.,-1.));
#6547=DIRECTION('center_axis',(0.,1.,0.));
#6548=DIRECTION('ref_axis',(1.,0.,0.));
#6549=DIRECTION('center_axis',(0.,1.,0.));
#6550=DIRECTION('ref_axis',(1.,0.,0.));
#6551=DIRECTION('center_axis',(0.,1.,0.));
#6552=DIRECTION('ref_axis',(0.,0.,1.));
#6553=DIRECTION('center_axis',(0.,-1.,0.));
#6554=DIRECTION('ref_axis',(1.,0.,0.));
#6555=DIRECTION('center_axis',(0.,-1.,0.));
#6556=DIRECTION('ref_axis',(1.,0.,0.));
#6557=DIRECTION('center_axis',(0.,-1.,0.));
#6558=DIRECTION('ref_axis',(1.,0.,0.));
#6559=DIRECTION('',(0.707106781186548,0.707106781186547,8.65956056235494E-17));
#6560=DIRECTION('center_axis',(0.,-1.,0.));
#6561=DIRECTION('ref_axis',(1.,0.,0.));
#6562=DIRECTION('center_axis',(0.,-1.,0.));
#6563=DIRECTION('ref_axis',(1.,0.,0.));
#6564=DIRECTION('',(0.,1.,0.));
#6565=DIRECTION('center_axis',(0.,1.,0.));
#6566=DIRECTION('ref_axis',(1.,0.,0.));
#6567=DIRECTION('center_axis',(0.,-1.,0.));
#6568=DIRECTION('ref_axis',(1.,0.,0.));
#6569=DIRECTION('',(-0.707106781186547,0.707106781186548,-8.65956056235493E-17));
#6570=DIRECTION('center_axis',(0.,-1.,0.));
#6571=DIRECTION('ref_axis',(0.,0.,-1.));
#6572=DIRECTION('center_axis',(0.,-1.,0.));
#6573=DIRECTION('ref_axis',(1.,0.,0.));
#6574=DIRECTION('center_axis',(0.,1.,0.));
#6575=DIRECTION('ref_axis',(1.,0.,0.));
#6576=DIRECTION('center_axis',(0.,1.,0.));
#6577=DIRECTION('ref_axis',(1.,0.,0.));
#6578=DIRECTION('',(-0.447213595499958,0.894427190999916,-5.47678698264203E-17));
#6579=DIRECTION('center_axis',(0.,-1.,0.));
#6580=DIRECTION('ref_axis',(1.,0.,0.));
#6581=DIRECTION('',(0.,1.,0.));
#8704=CARTESIAN_POINT('',(0.,0.,0.));
#8705=CARTESIAN_POINT('Origin',(0.144337567297406,-0.6,-0.25));
#8706=CARTESIAN_POINT('',(0.288675134594813,-0.6,0.));
#8707=CARTESIAN_POINT('',(0.144337567297406,-0.6,-0.25));
#8708=CARTESIAN_POINT('',(0.288675134594813,-0.6,0.));
#8709=CARTESIAN_POINT('',(0.144337567297406,-0.96,-0.25));
#8710=CARTESIAN_POINT('',(0.144337567297406,-0.6,-0.25));
#8711=CARTESIAN_POINT('',(0.288675134594813,-0.96,0.));
#8712=CARTESIAN_POINT('',(0.288675134594813,-0.96,0.));
#8713=CARTESIAN_POINT('',(0.288675134594813,-0.6,0.));
#8714=CARTESIAN_POINT('Origin',(-0.144337567297406,-0.6,-0.25));
#8715=CARTESIAN_POINT('',(-0.144337567297406,-0.6,-0.25));
#8716=CARTESIAN_POINT('',(0.144337567297406,-0.6,-0.25));
#8717=CARTESIAN_POINT('',(-0.144337567297406,-0.96,-0.25));
#8718=CARTESIAN_POINT('',(-0.144337567297406,-0.6,-0.25));
#8719=CARTESIAN_POINT('',(0.144337567297406,-0.96,-0.25));
#8720=CARTESIAN_POINT('Origin',(-0.288675134594813,-0.6,-8.32667268468867E-17));
#8721=CARTESIAN_POINT('',(-0.288675134594813,-0.6,-3.53525079574969E-17));
#8722=CARTESIAN_POINT('',(-0.144337567297406,-0.6,-0.25));
#8723=CARTESIAN_POINT('',(-0.288675134594813,-0.96,-5.55111512312578E-17));
#8724=CARTESIAN_POINT('',(-0.288675134594813,-0.6,-3.53525079574969E-17));
#8725=CARTESIAN_POINT('',(-0.144337567297406,-0.96,-0.25));
#8726=CARTESIAN_POINT('Origin',(-0.144337567297407,-0.6,0.25));
#8727=CARTESIAN_POINT('',(-0.144337567297407,-0.6,0.25));
#8728=CARTESIAN_POINT('',(-0.288675134594813,-0.6,-3.53525079574969E-17));
#8729=CARTESIAN_POINT('',(-0.144337567297407,-0.96,0.25));
#8730=CARTESIAN_POINT('',(-0.144337567297407,-0.6,0.25));
#8731=CARTESIAN_POINT('',(-0.288675134594813,-0.96,-3.53525079574969E-17));
#8732=CARTESIAN_POINT('Origin',(0.144337567297406,-0.6,0.25));
#8733=CARTESIAN_POINT('',(0.144337567297406,-0.6,0.25));
#8734=CARTESIAN_POINT('',(-0.144337567297407,-0.6,0.25));
#8735=CARTESIAN_POINT('',(0.144337567297406,-0.96,0.25));
#8736=CARTESIAN_POINT('',(0.144337567297406,-0.6,0.25));
#8737=CARTESIAN_POINT('',(-0.144337567297407,-0.96,0.25));
#8738=CARTESIAN_POINT('Origin',(0.288675134594813,-0.6,0.));
#8739=CARTESIAN_POINT('',(0.144337567297406,-0.6,0.25));
#8740=CARTESIAN_POINT('',(0.144337567297406,-0.96,0.25));
#8741=CARTESIAN_POINT('Origin',(0.,-0.6,0.));
#8742=CARTESIAN_POINT('Origin',(0.,-0.96,0.));
#8743=CARTESIAN_POINT('Origin',(0.,-1.8,0.));
#8744=CARTESIAN_POINT('',(-0.2942,-1.8,3.60291088309151E-17));
#8745=CARTESIAN_POINT('Origin',(0.,-1.8,0.));
#8746=CARTESIAN_POINT('Origin',(0.45,0.6,0.));
#8747=CARTESIAN_POINT('',(-0.45,0.6,-5.51091059616309E-17));
#8748=CARTESIAN_POINT('Origin',(0.,0.6,0.));
#8749=CARTESIAN_POINT('Origin',(0.,0.575,0.));
#8750=CARTESIAN_POINT('',(-0.5,0.55,-6.12323399573677E-17));
#8751=CARTESIAN_POINT('Origin',(0.,0.55,0.));
#8752=CARTESIAN_POINT('',(-0.475,0.575,-5.81707229594993E-17));
#8753=CARTESIAN_POINT('Origin',(0.,0.29,0.));
#8754=CARTESIAN_POINT('',(-0.5,0.0299999999999998,-6.12323399573677E-17));
#8755=CARTESIAN_POINT('Origin',(0.,0.0299999999999998,0.));
#8756=CARTESIAN_POINT('',(-0.5,0.29,-6.12323399573677E-17));
#8757=CARTESIAN_POINT('Origin',(0.,0.0150000000000001,0.));
#8758=CARTESIAN_POINT('',(-0.47,7.11236625150491E-17,-5.75583995599256E-17));
#8759=CARTESIAN_POINT('Origin',(0.,0.,0.));
#8760=CARTESIAN_POINT('',(-0.485,0.0150000000000001,-5.93953697586466E-17));
#8761=CARTESIAN_POINT('Origin',(0.32,0.,0.));
#8762=CARTESIAN_POINT('',(-0.32,-6.93889390390723E-18,-3.91886975727153E-17));
#8763=CARTESIAN_POINT('Origin',(0.,0.,0.));
#8764=CARTESIAN_POINT('Origin',(0.,-0.02,0.));
#8765=CARTESIAN_POINT('',(-0.2942,-0.0515999999999999,3.60291088309151E-17));
#8766=CARTESIAN_POINT('Origin',(0.,-0.0515999999999999,0.));
#8767=CARTESIAN_POINT('',(-0.31,-0.02,-3.7964050773568E-17));
#8768=CARTESIAN_POINT('Origin',(0.,-1.24,0.));
#8769=CARTESIAN_POINT('',(-0.2942,-1.24,-3.60291088309151E-17));
#9762=UNCERTAINTY_MEASURE_WITH_UNIT(LENGTH_MEASURE(0.001),#9814,
'DISTANCE_ACCURACY_VALUE',
'Maximum model space distance between geometric entities at asserted c
onnectivities');
#9777=UNCERTAINTY_MEASURE_WITH_UNIT(LENGTH_MEASURE(0.001),#9814,
'DISTANCE_ACCURACY_VALUE',
'Maximum model space distance between geometric entities at asserted c
onnectivities');
#9798=(
GEOMETRIC_REPRESENTATION_CONTEXT(3)
GLOBAL_UNCERTAINTY_ASSIGNED_CONTEXT((#9762))
GLOBAL_UNIT_ASSIGNED_CONTEXT((#9814,#9816,#9817))
REPRESENTATION_CONTEXT('','3D')
);
#9813=(
GEOMETRIC_REPRESENTATION_CONTEXT(3)
GLOBAL_UNCERTAINTY_ASSIGNED_CONTEXT((#9777))
GLOBAL_UNIT_ASSIGNED_CONTEXT((#9814,#9816,#9817))
REPRESENTATION_CONTEXT('','3D')
);
#9814=(
LENGTH_UNIT()
NAMED_UNIT(*)
SI_UNIT(.CENTI.,.METRE.)
);
#9816=(
NAMED_UNIT(*)
PLANE_ANGLE_UNIT()
SI_UNIT($,.RADIAN.)
);
#9817=(
NAMED_UNIT(*)
SI_UNIT($,.STERADIAN.)
SOLID_ANGLE_UNIT()
);
#9838=SHAPE_DEFINITION_REPRESENTATION(#9873,#9955);
#9873=PRODUCT_DEFINITION_SHAPE('',$,#9991);
#9955=SHAPE_REPRESENTATION('',(#5418),#9798);
#9970=PRODUCT_DEFINITION_CONTEXT('part definition',#10077,'design');
#9991=PRODUCT_DEFINITION('M6x18 mounting screw','M6x18 mounting screw',
#10026,#9970);
#10026=PRODUCT_DEFINITION_FORMATION('',$,#10099);
#10077=APPLICATION_CONTEXT(
'Core Data for Automotive Mechanical Design Process');
#10078=PRODUCT_CONTEXT('part definition',#10077,'mechanical');
#10099=PRODUCT('M6x18 mounting screw','M6x18 mounting screw',
'M6x18 mounting screw',(#10078));
#10184=COLOUR_RGB('Black',0.12,0.14,0.17);
#10185=FILL_AREA_STYLE_COLOUR('',#10184);
#10186=FILL_AREA_STYLE('',(#10185));
#10187=SURFACE_STYLE_FILL_AREA(#10186);
#10188=SURFACE_SIDE_STYLE('',(#10187));
#10189=SURFACE_STYLE_USAGE(.BOTH.,#10188);
#10190=PRESENTATION_STYLE_ASSIGNMENT((#10189));
ENDSEC;
END-ISO-10303-21;
